ISO-10303-21;
HEADER;
/* Generated by software containing ST-Developer
 * from STEP Tools, Inc. (www.steptools.com) 
 */

FILE_DESCRIPTION(
/* description */ ('Quick-return (Whitworth) mechanism'),
/* implementation_level */ '2;1');

FILE_NAME(
/* name */ 'Cap Screw - M4x16.step',
/* time_stamp */ '2026-10-28T03:25:57-07:00',
/* author */ (''),
/* organization */ (''),
/* preprocessor_version */ 'ST-DEVELOPER v20.2',
/* originating_system */ 'Autodesk Translation Framework v15.17.0.0',
/* authorisation */ '');

FILE_SCHEMA (('AUTOMOTIVE_DESIGN { 1 0 10303 214 3 1 1 }'));
ENDSEC;

DATA;
#10=MECHANICAL_DESIGN_GEOMETRIC_PRESENTATION_REPRESENTATION('',(#519),#14878);
#11=ORIENTED_CLOSED_SHELL('',*,#7874,.F.);
#14=BREP_WITH_VOIDS('Body1',#7873,(#11));
#353=CONICAL_SURFACE('',#8957,0.325,0.785398163397448);
#354=CONICAL_SURFACE('',#8961,0.335,0.785398163397448);
#355=CONICAL_SURFACE('',#8965,0.21,0.463647609000806);
#356=CONICAL_SURFACE('',#8969,0.18,0.785398163397448);
#423=SHAPE_REPRESENTATION_RELATIONSHIP('SRR','None',#15093,#467);
#467=ADVANCED_BREP_SHAPE_REPRESENTATION('',(#14),#14850);
#519=STYLED_ITEM('',(#15413),#14);
#724=FACE_BOUND('',#1905,.T.);
#901=PLANE('',#8955);
#902=PLANE('',#8963);
#903=PLANE('',#8971);
#904=PLANE('',#8972);
#905=PLANE('',#8973);
#906=PLANE('',#8974);
#907=PLANE('',#8975);
#908=PLANE('',#8976);
#909=PLANE('',#8977);
#910=PLANE('',#8978);
#911=PLANE('',#8979);
#1301=FACE_OUTER_BOUND('',#1900,.T.);
#1302=FACE_OUTER_BOUND('',#1901,.T.);
#1303=FACE_OUTER_BOUND('',#1902,.T.);
#1304=FACE_OUTER_BOUND('',#1903,.T.);
#1305=FACE_OUTER_BOUND('',#1904,.T.);
#1306=FACE_OUTER_BOUND('',#1906,.T.);
#1307=FACE_OUTER_BOUND('',#1907,.T.);
#1308=FACE_OUTER_BOUND('',#1908,.T.);
#1309=FACE_OUTER_BOUND('',#1909,.T.);
#1310=FACE_OUTER_BOUND('',#1910,.T.);
#1311=FACE_OUTER_BOUND('',#1911,.T.);
#1312=FACE_OUTER_BOUND('',#1912,.T.);
#1313=FACE_OUTER_BOUND('',#1913,.T.);
#1314=FACE_OUTER_BOUND('',#1914,.T.);
#1315=FACE_OUTER_BOUND('',#1915,.T.);
#1316=FACE_OUTER_BOUND('',#1916,.T.);
#1317=FACE_OUTER_BOUND('',#1917,.T.);
#1900=EDGE_LOOP('',(#6318));
#1901=EDGE_LOOP('',(#6319,#6320,#6321,#6322));
#1902=EDGE_LOOP('',(#6323,#6324,#6325,#6326));
#1903=EDGE_LOOP('',(#6327,#6328,#6329,#6330));
#1904=EDGE_LOOP('',(#6331));
#1905=EDGE_LOOP('',(#6332));
#1906=EDGE_LOOP('',(#6333,#6334,#6335,#6336));
#1907=EDGE_LOOP('',(#6337,#6338,#6339,#6340));
#1908=EDGE_LOOP('',(#6341,#6342,#6343,#6344));
#1909=EDGE_LOOP('',(#6345));
#1910=EDGE_LOOP('',(#6346,#6347,#6348,#6349));
#1911=EDGE_LOOP('',(#6350,#6351,#6352,#6353));
#1912=EDGE_LOOP('',(#6354,#6355,#6356,#6357));
#1913=EDGE_LOOP('',(#6358,#6359,#6360,#6361));
#1914=EDGE_LOOP('',(#6362,#6363,#6364,#6365));
#1915=EDGE_LOOP('',(#6366,#6367,#6368,#6369));
#1916=EDGE_LOOP('',(#6370,#6371,#6372,#6373,#6374,#6375));
#1917=EDGE_LOOP('',(#6376,#6377,#6378,#6379,#6380,#6381));
#2381=LINE('',#13663,#2904);
#2382=LINE('',#13667,#2905);
#2383=LINE('',#13671,#2906);
#2384=LINE('',#13678,#2907);
#2385=LINE('',#13682,#2908);
#2386=LINE('',#13686,#2909);
#2387=LINE('',#13691,#2910);
#2388=LINE('',#13693,#2911);
#2389=LINE('',#13695,#2912);
#2390=LINE('',#13696,#2913);
#2391=LINE('',#13699,#2914);
#2392=LINE('',#13701,#2915);
#2393=LINE('',#13702,#2916);
#2394=LINE('',#13705,#2917);
#2395=LINE('',#13707,#2918);
#2396=LINE('',#13708,#2919);
#2397=LINE('',#13711,#2920);
#2398=LINE('',#13713,#2921);
#2399=LINE('',#13714,#2922);
#2400=LINE('',#13717,#2923);
#2401=LINE('',#13719,#2924);
#2402=LINE('',#13720,#2925);
#2403=LINE('',#13722,#2926);
#2404=LINE('',#13723,#2927);
#2904=VECTOR('',#10758,0.325);
#2905=VECTOR('',#10763,0.35);
#2906=VECTOR('',#10768,0.335);
#2907=VECTOR('',#10777,0.21);
#2908=VECTOR('',#10782,0.2);
#2909=VECTOR('',#10787,0.18);
#2910=VECTOR('',#10792,1.);
#2911=VECTOR('',#10793,1.);
#2912=VECTOR('',#10794,1.);
#2913=VECTOR('',#10795,1.);
#2914=VECTOR('',#10798,1.);
#2915=VECTOR('',#10799,1.);
#2916=VECTOR('',#10800,1.);
#2917=VECTOR('',#10803,1.);
#2918=VECTOR('',#10804,1.);
#2919=VECTOR('',#10805,1.);
#2920=VECTOR('',#10808,1.);
#2921=VECTOR('',#10809,1.);
#2922=VECTOR('',#10810,1.);
#2923=VECTOR('',#10813,1.);
#2924=VECTOR('',#10814,1.);
#2925=VECTOR('',#10815,1.);
#2926=VECTOR('',#10818,1.);
#2927=VECTOR('',#10819,1.);
#3502=CIRCLE('',#8956,0.3);
#3503=CIRCLE('',#8958,0.35);
#3504=CIRCLE('',#8960,0.35);
#3505=CIRCLE('',#8962,0.32);
#3506=CIRCLE('',#8964,0.22);
#3507=CIRCLE('',#8966,0.1954);
#3508=CIRCLE('',#8968,0.1954);
#3509=CIRCLE('',#8970,0.16);
#3994=VERTEX_POINT('',#13658);
#3995=VERTEX_POINT('',#13661);
#3996=VERTEX_POINT('',#13665);
#3997=VERTEX_POINT('',#13669);
#3998=VERTEX_POINT('',#13673);
#3999=VERTEX_POINT('',#13676);
#4000=VERTEX_POINT('',#13680);
#4001=VERTEX_POINT('',#13684);
#4002=VERTEX_POINT('',#13689);
#4003=VERTEX_POINT('',#13690);
#4004=VERTEX_POINT('',#13692);
#4005=VERTEX_POINT('',#13694);
#4006=VERTEX_POINT('',#13698);
#4007=VERTEX_POINT('',#13700);
#4008=VERTEX_POINT('',#13704);
#4009=VERTEX_POINT('',#13706);
#4010=VERTEX_POINT('',#13710);
#4011=VERTEX_POINT('',#13712);
#4012=VERTEX_POINT('',#13716);
#4013=VERTEX_POINT('',#13718);
#4816=EDGE_CURVE('',#3994,#3994,#3502,.T.);
#4817=EDGE_CURVE('',#3995,#3995,#3503,.T.);
#4818=EDGE_CURVE('',#3995,#3994,#2381,.T.);
#4819=EDGE_CURVE('',#3996,#3996,#3504,.T.);
#4820=EDGE_CURVE('',#3996,#3995,#2382,.T.);
#4821=EDGE_CURVE('',#3997,#3997,#3505,.T.);
#4822=EDGE_CURVE('',#3997,#3996,#2383,.T.);
#4823=EDGE_CURVE('',#3998,#3998,#3506,.T.);
#4824=EDGE_CURVE('',#3999,#3999,#3507,.F.);
#4825=EDGE_CURVE('',#3999,#3998,#2384,.T.);
#4826=EDGE_CURVE('',#4000,#4000,#3508,.F.);
#4827=EDGE_CURVE('',#4000,#3999,#2385,.T.);
#4828=EDGE_CURVE('',#4001,#4001,#3509,.T.);
#4829=EDGE_CURVE('',#4001,#4000,#2386,.T.);
#4830=EDGE_CURVE('',#4002,#4003,#2387,.T.);
#4831=EDGE_CURVE('',#4003,#4004,#2388,.T.);
#4832=EDGE_CURVE('',#4004,#4005,#2389,.T.);
#4833=EDGE_CURVE('',#4002,#4005,#2390,.T.);
#4834=EDGE_CURVE('',#4003,#4006,#2391,.T.);
#4835=EDGE_CURVE('',#4006,#4007,#2392,.T.);
#4836=EDGE_CURVE('',#4007,#4004,#2393,.T.);
#4837=EDGE_CURVE('',#4006,#4008,#2394,.T.);
#4838=EDGE_CURVE('',#4008,#4009,#2395,.T.);
#4839=EDGE_CURVE('',#4009,#4007,#2396,.T.);
#4840=EDGE_CURVE('',#4008,#4010,#2397,.T.);
#4841=EDGE_CURVE('',#4010,#4011,#2398,.T.);
#4842=EDGE_CURVE('',#4011,#4009,#2399,.T.);
#4843=EDGE_CURVE('',#4010,#4012,#2400,.T.);
#4844=EDGE_CURVE('',#4012,#4013,#2401,.T.);
#4845=EDGE_CURVE('',#4013,#4011,#2402,.T.);
#4846=EDGE_CURVE('',#4012,#4002,#2403,.T.);
#4847=EDGE_CURVE('',#4005,#4013,#2404,.T.);
#6318=ORIENTED_EDGE('',*,*,#4816,.F.);
#6319=ORIENTED_EDGE('',*,*,#4817,.F.);
#6320=ORIENTED_EDGE('',*,*,#4818,.T.);
#6321=ORIENTED_EDGE('',*,*,#4816,.T.);
#6322=ORIENTED_EDGE('',*,*,#4818,.F.);
#6323=ORIENTED_EDGE('',*,*,#4819,.F.);
#6324=ORIENTED_EDGE('',*,*,#4820,.T.);
#6325=ORIENTED_EDGE('',*,*,#4817,.T.);
#6326=ORIENTED_EDGE('',*,*,#4820,.F.);
#6327=ORIENTED_EDGE('',*,*,#4821,.F.);
#6328=ORIENTED_EDGE('',*,*,#4822,.T.);
#6329=ORIENTED_EDGE('',*,*,#4819,.T.);
#6330=ORIENTED_EDGE('',*,*,#4822,.F.);
#6331=ORIENTED_EDGE('',*,*,#4821,.T.);
#6332=ORIENTED_EDGE('',*,*,#4823,.F.);
#6333=ORIENTED_EDGE('',*,*,#4824,.F.);
#6334=ORIENTED_EDGE('',*,*,#4825,.T.);
#6335=ORIENTED_EDGE('',*,*,#4823,.T.);
#6336=ORIENTED_EDGE('',*,*,#4825,.F.);
#6337=ORIENTED_EDGE('',*,*,#4826,.F.);
#6338=ORIENTED_EDGE('',*,*,#4827,.T.);
#6339=ORIENTED_EDGE('',*,*,#4824,.T.);
#6340=ORIENTED_EDGE('',*,*,#4827,.F.);
#6341=ORIENTED_EDGE('',*,*,#4828,.F.);
#6342=ORIENTED_EDGE('',*,*,#4829,.T.);
#6343=ORIENTED_EDGE('',*,*,#4826,.T.);
#6344=ORIENTED_EDGE('',*,*,#4829,.F.);
#6345=ORIENTED_EDGE('',*,*,#4828,.T.);
#6346=ORIENTED_EDGE('',*,*,#4830,.T.);
#6347=ORIENTED_EDGE('',*,*,#4831,.T.);
#6348=ORIENTED_EDGE('',*,*,#4832,.T.);
#6349=ORIENTED_EDGE('',*,*,#4833,.F.);
#6350=ORIENTED_EDGE('',*,*,#4834,.T.);
#6351=ORIENTED_EDGE('',*,*,#4835,.T.);
#6352=ORIENTED_EDGE('',*,*,#4836,.T.);
#6353=ORIENTED_EDGE('',*,*,#4831,.F.);
#6354=ORIENTED_EDGE('',*,*,#4837,.T.);
#6355=ORIENTED_EDGE('',*,*,#4838,.T.);
#6356=ORIENTED_EDGE('',*,*,#4839,.T.);
#6357=ORIENTED_EDGE('',*,*,#4835,.F.);
#6358=ORIENTED_EDGE('',*,*,#4840,.T.);
#6359=ORIENTED_EDGE('',*,*,#4841,.T.);
#6360=ORIENTED_EDGE('',*,*,#4842,.T.);
#6361=ORIENTED_EDGE('',*,*,#4838,.F.);
#6362=ORIENTED_EDGE('',*,*,#4843,.T.);
#6363=ORIENTED_EDGE('',*,*,#4844,.T.);
#6364=ORIENTED_EDGE('',*,*,#4845,.T.);
#6365=ORIENTED_EDGE('',*,*,#4841,.F.);
#6366=ORIENTED_EDGE('',*,*,#4846,.T.);
#6367=ORIENTED_EDGE('',*,*,#4833,.T.);
#6368=ORIENTED_EDGE('',*,*,#4847,.T.);
#6369=ORIENTED_EDGE('',*,*,#4844,.F.);
#6370=ORIENTED_EDGE('',*,*,#4846,.F.);
#6371=ORIENTED_EDGE('',*,*,#4843,.F.);
#6372=ORIENTED_EDGE('',*,*,#4840,.F.);
#6373=ORIENTED_EDGE('',*,*,#4837,.F.);
#6374=ORIENTED_EDGE('',*,*,#4834,.F.);
#6375=ORIENTED_EDGE('',*,*,#4830,.F.);
#6376=ORIENTED_EDGE('',*,*,#4847,.F.);
#6377=ORIENTED_EDGE('',*,*,#4832,.F.);
#6378=ORIENTED_EDGE('',*,*,#4836,.F.);
#6379=ORIENTED_EDGE('',*,*,#4839,.F.);
#6380=ORIENTED_EDGE('',*,*,#4842,.F.);
#6381=ORIENTED_EDGE('',*,*,#4845,.F.);
#7323=CYLINDRICAL_SURFACE('',#8959,0.35);
#7324=CYLINDRICAL_SURFACE('',#8967,0.1954);
#7632=ADVANCED_FACE('',(#1301),#901,.T.);
#7633=ADVANCED_FACE('',(#1302),#353,.T.);
#7634=ADVANCED_FACE('',(#1303),#7323,.T.);
#7635=ADVANCED_FACE('',(#1304),#354,.T.);
#7636=ADVANCED_FACE('',(#1305,#724),#902,.T.);
#7637=ADVANCED_FACE('',(#1306),#355,.T.);
#7638=ADVANCED_FACE('',(#1307),#7324,.T.);
#7639=ADVANCED_FACE('',(#1308),#356,.T.);
#7640=ADVANCED_FACE('',(#1309),#903,.T.);
#7641=ADVANCED_FACE('',(#1310),#904,.F.);
#7642=ADVANCED_FACE('',(#1311),#905,.F.);
#7643=ADVANCED_FACE('',(#1312),#906,.F.);
#7644=ADVANCED_FACE('',(#1313),#907,.F.);
#7645=ADVANCED_FACE('',(#1314),#908,.F.);
#7646=ADVANCED_FACE('',(#1315),#909,.F.);
#7647=ADVANCED_FACE('',(#1316),#910,.F.);
#7648=ADVANCED_FACE('',(#1317),#911,.F.);
#7873=CLOSED_SHELL('',(#7632,#7633,#7634,#7635,#7636,#7637,#7638,#7639,
#7640));
#7874=CLOSED_SHELL('',(#7641,#7642,#7643,#7644,#7645,#7646,#7647,#7648));
#8954=AXIS2_PLACEMENT_3D('',#13656,#10748,#10749);
#8955=AXIS2_PLACEMENT_3D('',#13657,#10750,#10751);
#8956=AXIS2_PLACEMENT_3D('',#13659,#10752,#10753);
#8957=AXIS2_PLACEMENT_3D('',#13660,#10754,#10755);
#8958=AXIS2_PLACEMENT_3D('',#13662,#10756,#10757);
#8959=AXIS2_PLACEMENT_3D('',#13664,#10759,#10760);
#8960=AXIS2_PLACEMENT_3D('',#13666,#10761,#10762);
#8961=AXIS2_PLACEMENT_3D('',#13668,#10764,#10765);
#8962=AXIS2_PLACEMENT_3D('',#13670,#10766,#10767);
#8963=AXIS2_PLACEMENT_3D('',#13672,#10769,#10770);
#8964=AXIS2_PLACEMENT_3D('',#13674,#10771,#10772);
#8965=AXIS2_PLACEMENT_3D('',#13675,#10773,#10774);
#8966=AXIS2_PLACEMENT_3D('',#13677,#10775,#10776);
#8967=AXIS2_PLACEMENT_3D('',#13679,#10778,#10779);
#8968=AXIS2_PLACEMENT_3D('',#13681,#10780,#10781);
#8969=AXIS2_PLACEMENT_3D('',#13683,#10783,#10784);
#8970=AXIS2_PLACEMENT_3D('',#13685,#10785,#10786);
#8971=AXIS2_PLACEMENT_3D('',#13687,#10788,#10789);
#8972=AXIS2_PLACEMENT_3D('',#13688,#10790,#10791);
#8973=AXIS2_PLACEMENT_3D('',#13697,#10796,#10797);
#8974=AXIS2_PLACEMENT_3D('',#13703,#10801,#10802);
#8975=AXIS2_PLACEMENT_3D('',#13709,#10806,#10807);
#8976=AXIS2_PLACEMENT_3D('',#13715,#10811,#10812);
#8977=AXIS2_PLACEMENT_3D('',#13721,#10816,#10817);
#8978=AXIS2_PLACEMENT_3D('',#13724,#10820,#10821);
#8979=AXIS2_PLACEMENT_3D('',#13725,#10822,#10823);
#10748=DIRECTION('axis',(0.,0.,1.));
#10749=DIRECTION('refdir',(1.,0.,0.));
#10750=DIRECTION('center_axis',(0.,1.,0.));
#10751=DIRECTION('ref_axis',(0.,0.,1.));
#10752=DIRECTION('center_axis',(0.,-1.,0.));
#10753=DIRECTION('ref_axis',(1.,0.,0.));
#10754=DIRECTION('center_axis',(0.,-1.,0.));
#10755=DIRECTION('ref_axis',(1.,0.,0.));
#10756=DIRECTION('center_axis',(0.,-1.,0.));
#10757=DIRECTION('ref_axis',(1.,0.,0.));
#10758=DIRECTION('',(0.707106781186547,0.707106781186548,8.65956056235493E-17));
#10759=DIRECTION('center_axis',(0.,-1.,0.));
#10760=DIRECTION('ref_axis',(1.,0.,0.));
#10761=DIRECTION('center_axis',(0.,-1.,0.));
#10762=DIRECTION('ref_axis',(1.,0.,0.));
#10763=DIRECTION('',(0.,1.,0.));
#10764=DIRECTION('center_axis',(0.,1.,0.));
#10765=DIRECTION('ref_axis',(1.,0.,0.));
#10766=DIRECTION('center_axis',(0.,-1.,0.));
#10767=DIRECTION('ref_axis',(1.,0.,0.));
#10768=DIRECTION('',(-0.707106781186547,0.707106781186548,-8.65956056235493E-17));
#10769=DIRECTION('center_axis',(0.,-1.,0.));
#10770=DIRECTION('ref_axis',(0.,0.,-1.));
#10771=DIRECTION('center_axis',(0.,-1.,0.));
#10772=DIRECTION('ref_axis',(1.,0.,0.));
#10773=DIRECTION('center_axis',(0.,1.,0.));
#10774=DIRECTION('ref_axis',(1.,0.,0.));
#10775=DIRECTION('center_axis',(0.,1.,0.));
#10776=DIRECTION('ref_axis',(1.,0.,0.));
#10777=DIRECTION('',(-0.447213595499958,0.894427190999916,-5.47678698264203E-17));
#10778=DIRECTION('center_axis',(0.,-1.,0.));
#10779=DIRECTION('ref_axis',(1.,0.,0.));
#10780=DIRECTION('center_axis',(0.,1.,0.));
#10781=DIRECTION('ref_axis',(1.,0.,0.));
#10782=DIRECTION('',(0.,1.,0.));
#10783=DIRECTION('center_axis',(0.,1.,0.));
#10784=DIRECTION('ref_axis',(1.,0.,0.));
#10785=DIRECTION('center_axis',(0.,-1.,0.));
#10786=DIRECTION('ref_axis',(1.,0.,0.));
#10787=DIRECTION('',(-0.707106781186547,0.707106781186548,-8.65956056235493E-17));
#10788=DIRECTION('center_axis',(0.,-1.,0.));
#10789=DIRECTION('ref_axis',(0.,0.,-1.));
#10790=DIRECTION('center_axis',(0.866025403784439,0.,-0.5));
#10791=DIRECTION('ref_axis',(0.5,0.,0.866025403784439));
#10792=DIRECTION('',(-0.5,0.,-0.866025403784439));
#10793=DIRECTION('',(0.,-1.,0.));
#10794=DIRECTION('',(0.5,0.,0.866025403784439));
#10795=DIRECTION('',(0.,-1.,0.));
#10796=DIRECTION('center_axis',(1.60246890531964E-16,0.,-1.));
#10797=DIRECTION('ref_axis',(1.,0.,1.60246890531964E-16));
#10798=DIRECTION('',(-1.,0.,-1.60246890531964E-16));
#10799=DIRECTION('',(0.,-1.,0.));
#10800=DIRECTION('',(1.,0.,1.60246890531964E-16));
#10801=DIRECTION('center_axis',(-0.866025403784439,0.,-0.5));
#10802=DIRECTION('ref_axis',(0.5,0.,-0.866025403784439));
#10803=DIRECTION('',(-0.5,0.,0.866025403784439));
#10804=DIRECTION('',(0.,-1.,0.));
#10805=DIRECTION('',(0.5,0.,-0.866025403784439));
#10806=DIRECTION('center_axis',(-0.866025403784439,0.,0.5));
#10807=DIRECTION('ref_axis',(-0.5,0.,-0.866025403784439));
#10808=DIRECTION('',(0.5,0.,0.866025403784439));
#10809=DIRECTION('',(0.,-1.,0.));
#10810=DIRECTION('',(-0.5,0.,-0.866025403784439));
#10811=DIRECTION('center_axis',(-1.60246890531964E-16,0.,1.));
#10812=DIRECTION('ref_axis',(-1.,0.,-1.60246890531964E-16));
#10813=DIRECTION('',(1.,0.,1.60246890531964E-16));
#10814=DIRECTION('',(0.,-1.,0.));
#10815=DIRECTION('',(-1.,0.,-1.60246890531964E-16));
#10816=DIRECTION('center_axis',(0.866025403784439,0.,0.5));
#10817=DIRECTION('ref_axis',(-0.5,0.,0.866025403784439));
#10818=DIRECTION('',(0.5,0.,-0.866025403784439));
#10819=DIRECTION('',(-0.5,0.,0.866025403784439));
#10820=DIRECTION('center_axis',(0.,1.,0.));
#10821=DIRECTION('ref_axis',(1.,0.,0.));
#10822=DIRECTION('center_axis',(0.,-1.,0.));
#10823=DIRECTION('ref_axis',(0.,0.,-1.));
#13656=CARTESIAN_POINT('',(0.,0.,0.));
#13657=CARTESIAN_POINT('Origin',(0.3,0.4,0.));
#13658=CARTESIAN_POINT('',(-0.3,0.4,-3.67394039744206E-17));
#13659=CARTESIAN_POINT('Origin',(0.,0.4,0.));
#13660=CARTESIAN_POINT('Origin',(0.,0.375,0.));
#13661=CARTESIAN_POINT('',(-0.35,0.35,-4.28626379701573E-17));
#13662=CARTESIAN_POINT('Origin',(0.,0.35,0.));
#13663=CARTESIAN_POINT('',(-0.325,0.375,-3.9801020972289E-17));
#13664=CARTESIAN_POINT('Origin',(0.,0.19,0.));
#13665=CARTESIAN_POINT('',(-0.35,0.03,-4.28626379701574E-17));
#13666=CARTESIAN_POINT('Origin',(0.,0.03,0.));
#13667=CARTESIAN_POINT('',(-0.35,0.19,-4.28626379701574E-17));
#13668=CARTESIAN_POINT('Origin',(0.,0.0149999999999999,0.));
#13669=CARTESIAN_POINT('',(-0.32,-3.29597460435593E-17,-3.91886975727153E-17));
#13670=CARTESIAN_POINT('Origin',(0.,0.,0.));
#13671=CARTESIAN_POINT('',(-0.335,0.0149999999999999,-4.10256677714363E-17));
#13672=CARTESIAN_POINT('Origin',(0.22,0.,0.));
#13673=CARTESIAN_POINT('',(-0.22,-6.93889390390723E-18,-2.69422295812418E-17));
#13674=CARTESIAN_POINT('Origin',(0.,0.,0.));
#13675=CARTESIAN_POINT('Origin',(0.,-0.02,0.));
#13676=CARTESIAN_POINT('',(-0.1954,-0.0492,2.39295984553393E-17));
#13677=CARTESIAN_POINT('Origin',(0.,-0.0492,0.));
#13678=CARTESIAN_POINT('',(-0.21,-0.02,-2.57175827820944E-17));
#13679=CARTESIAN_POINT('Origin',(0.,-0.8,0.));
#13680=CARTESIAN_POINT('',(-0.1954,-1.5646,2.39295984553393E-17));
#13681=CARTESIAN_POINT('Origin',(0.,-1.5646,0.));
#13682=CARTESIAN_POINT('',(-0.1954,-0.8,-2.39295984553393E-17));
#13683=CARTESIAN_POINT('Origin',(0.,-1.58,0.));
#13684=CARTESIAN_POINT('',(-0.16,-1.6,-1.95943487863577E-17));
#13685=CARTESIAN_POINT('Origin',(0.,-1.6,0.));
#13686=CARTESIAN_POINT('',(-0.18,-1.58,-2.20436423846524E-17));
#13687=CARTESIAN_POINT('Origin',(0.,-1.6,0.));
#13688=CARTESIAN_POINT('Origin',(0.0866025403784439,-0.4,-0.15));
#13689=CARTESIAN_POINT('',(0.173205080756888,-0.4,0.));
#13690=CARTESIAN_POINT('',(0.0866025403784439,-0.4,-0.15));
#13691=CARTESIAN_POINT('',(0.173205080756888,-0.4,0.));
#13692=CARTESIAN_POINT('',(0.0866025403784439,-0.64,-0.15));
#13693=CARTESIAN_POINT('',(0.0866025403784439,-0.4,-0.15));
#13694=CARTESIAN_POINT('',(0.173205080756888,-0.64,0.));
#13695=CARTESIAN_POINT('',(0.173205080756888,-0.64,0.));
#13696=CARTESIAN_POINT('',(0.173205080756888,-0.4,0.));
#13697=CARTESIAN_POINT('Origin',(-0.0866025403784438,-0.4,-0.15));
#13698=CARTESIAN_POINT('',(-0.0866025403784438,-0.4,-0.15));
#13699=CARTESIAN_POINT('',(0.0866025403784439,-0.4,-0.15));
#13700=CARTESIAN_POINT('',(-0.0866025403784438,-0.64,-0.15));
#13701=CARTESIAN_POINT('',(-0.0866025403784438,-0.4,-0.15));
#13702=CARTESIAN_POINT('',(0.0866025403784439,-0.64,-0.15));
#13703=CARTESIAN_POINT('Origin',(-0.173205080756888,-0.4,-2.77555756156289E-17));
#13704=CARTESIAN_POINT('',(-0.173205080756888,-0.4,-2.12115047744981E-17));
#13705=CARTESIAN_POINT('',(-0.0866025403784438,-0.4,-0.15));
#13706=CARTESIAN_POINT('',(-0.173205080756888,-0.64,-2.77555756156289E-17));
#13707=CARTESIAN_POINT('',(-0.173205080756888,-0.4,-2.12115047744981E-17));
#13708=CARTESIAN_POINT('',(-0.0866025403784438,-0.64,-0.15));
#13709=CARTESIAN_POINT('Origin',(-0.0866025403784439,-0.4,0.15));
#13710=CARTESIAN_POINT('',(-0.0866025403784439,-0.4,0.15));
#13711=CARTESIAN_POINT('',(-0.173205080756888,-0.4,-2.12115047744981E-17));
#13712=CARTESIAN_POINT('',(-0.0866025403784439,-0.64,0.15));
#13713=CARTESIAN_POINT('',(-0.0866025403784439,-0.4,0.15));
#13714=CARTESIAN_POINT('',(-0.173205080756888,-0.64,-2.12115047744981E-17));
#13715=CARTESIAN_POINT('Origin',(0.0866025403784439,-0.4,0.15));
#13716=CARTESIAN_POINT('',(0.0866025403784439,-0.4,0.15));
#13717=CARTESIAN_POINT('',(-0.0866025403784439,-0.4,0.15));
#13718=CARTESIAN_POINT('',(0.0866025403784439,-0.64,0.15));
#13719=CARTESIAN_POINT('',(0.0866025403784439,-0.4,0.15));
#13720=CARTESIAN_POINT('',(-0.0866025403784439,-0.64,0.15));
#13721=CARTESIAN_POINT('Origin',(0.173205080756888,-0.4,0.));
#13722=CARTESIAN_POINT('',(0.0866025403784439,-0.4,0.15));
#13723=CARTESIAN_POINT('',(0.0866025403784439,-0.64,0.15));
#13724=CARTESIAN_POINT('Origin',(0.,-0.4,-2.77555756156289E-17));
#13725=CARTESIAN_POINT('Origin',(0.,-0.64,-2.77555756156289E-17));
#14796=UNCERTAINTY_MEASURE_WITH_UNIT(LENGTH_MEASURE(0.001),#14879,
'DISTANCE_ACCURACY_VALUE',
'Maximum model space distance between geometric entities at asserted c
onnectivities');
#14824=UNCERTAINTY_MEASURE_WITH_UNIT(LENGTH_MEASURE(0.001),#14879,
'DISTANCE_ACCURACY_VALUE',
'Maximum model space distance between geometric entities at asserted c
onnectivities');
#14850=(
GEOMETRIC_REPRESENTATION_CONTEXT(3)
GLOBAL_UNCERTAINTY_ASSIGNED_CONTEXT((#14796))
GLOBAL_UNIT_ASSIGNED_CONTEXT((#14879,#14881,#14882))
REPRESENTATION_CONTEXT('','3D')
);
#14878=(
GEOMETRIC_REPRESENTATION_CONTEXT(3)
GLOBAL_UNCERTAINTY_ASSIGNED_CONTEXT((#14824))
GLOBAL_UNIT_ASSIGNED_CONTEXT((#14879,#14881,#14882))
REPRESENTATION_CONTEXT('','3D')
);
#14879=(
LENGTH_UNIT()
NAMED_UNIT(*)
SI_UNIT(.CENTI.,.METRE.)
);
#14881=(
NAMED_UNIT(*)
PLANE_ANGLE_UNIT()
SI_UNIT($,.RADIAN.)
);
#14882=(
NAMED_UNIT(*)
SI_UNIT($,.STERADIAN.)
SOLID_ANGLE_UNIT()
);
#14908=SHAPE_DEFINITION_REPRESENTATION(#14966,#15093);
#14966=PRODUCT_DEFINITION_SHAPE('',$,#15147);
#15093=SHAPE_REPRESENTATION('',(#8954),#14850);
#15121=PRODUCT_DEFINITION_CONTEXT('part definition',#15282,'design');
#15147=PRODUCT_DEFINITION('Cap Screw - M4x16','Cap Screw - M4x16',#15200,
#15121);
#15200=PRODUCT_DEFINITION_FORMATION('',$,#15309);
#15282=APPLICATION_CONTEXT(
'Core Data for Automotive Mechanical Design Process');
#15283=PRODUCT_CONTEXT('part definition',#15282,'mechanical');
#15309=PRODUCT('Cap Screw - M4x16','Cap Screw - M4x16',
'Cap Screw - M4x16',(#15283));
#15407=COLOUR_RGB('Black',0.12,0.14,0.17);
#15408=FILL_AREA_STYLE_COLOUR('',#15407);
#15409=FILL_AREA_STYLE('',(#15408));
#15410=SURFACE_STYLE_FILL_AREA(#15409);
#15411=SURFACE_SIDE_STYLE('',(#15410));
#15412=SURFACE_STYLE_USAGE(.BOTH.,#15411);
#15413=PRESENTATION_STYLE_ASSIGNMENT((#15412));
ENDSEC;
END-ISO-10303-21;
